ISO-10303-21;
HEADER;
/* Generated by software containing ST-Developer
 * from STEP Tools, Inc. (www.steptools.com) 
 */

FILE_DESCRIPTION(
/* description */ (''),
/* implementation_level */ '2;1');

FILE_NAME(
/* name */ 'Front_Block.step',
/* time_stamp */ '2026-10-19T01:17:59+06:00',
/* author */ (''),
/* organization */ (''),
/* preprocessor_version */ 'ST-DEVELOPER v20.2',
/* originating_system */ 'Autodesk Translation Framework v15.15.0.0',
/* authorisation */ '');

FILE_SCHEMA (('AUTOMOTIVE_DESIGN { 1 0 10303 214 3 1 1 }'));
ENDSEC;

DATA;
#10=MECHANICAL_DESIGN_GEOMETRIC_PRESENTATION_REPRESENTATION('',(#751),#48369);
#620=SHAPE_REPRESENTATION_RELATIONSHIP('SRR','None',#48420,#631);
#631=ADVANCED_BREP_SHAPE_REPRESENTATION('',(#777),#48365);
#723=FACE_BOUND('',#3332,.T.);
#724=FACE_BOUND('',#3334,.T.);
#751=STYLED_ITEM('',(#48496),#777);
#777=MANIFOLD_SOLID_BREP('Front_Block',#20130);
#1186=CYLINDRICAL_SURFACE('',#21810,17.5);
#2194=FACE_OUTER_BOUND('',#3326,.T.);
#2195=FACE_OUTER_BOUND('',#3327,.T.);
#2196=FACE_OUTER_BOUND('',#3328,.T.);
#2197=FACE_OUTER_BOUND('',#3329,.T.);
#2198=FACE_OUTER_BOUND('',#3330,.T.);
#2199=FACE_OUTER_BOUND('',#3331,.T.);
#2200=FACE_OUTER_BOUND('',#3333,.T.);
#3326=EDGE_LOOP('',(#18241,#18242,#18243,#18244));
#3327=EDGE_LOOP('',(#18245,#18246,#18247,#18248));
#3328=EDGE_LOOP('',(#18249,#18250,#18251,#18252));
#3329=EDGE_LOOP('',(#18253,#18254,#18255,#18256));
#3330=EDGE_LOOP('',(#18257,#18258,#18259,#18260));
#3331=EDGE_LOOP('',(#18261,#18262,#18263,#18264));
#3332=EDGE_LOOP('',(#18265));
#3333=EDGE_LOOP('',(#18266,#18267,#18268,#18269));
#3334=EDGE_LOOP('',(#18270));
#3951=CIRCLE('',#21811,17.5);
#3952=CIRCLE('',#21812,17.5);
#5769=LINE('',#48029,#7650);
#5770=LINE('',#48034,#7651);
#5771=LINE('',#48036,#7652);
#5772=LINE('',#48038,#7653);
#5773=LINE('',#48039,#7654);
#5774=LINE('',#48042,#7655);
#5775=LINE('',#48044,#7656);
#5776=LINE('',#48045,#7657);
#5777=LINE('',#48048,#7658);
#5778=LINE('',#48050,#7659);
#5779=LINE('',#48051,#7660);
#5780=LINE('',#48053,#7661);
#5781=LINE('',#48054,#7662);
#7650=VECTOR('',#26814,17.5);
#7651=VECTOR('',#26819,10.);
#7652=VECTOR('',#26820,10.);
#7653=VECTOR('',#26821,10.);
#7654=VECTOR('',#26822,10.);
#7655=VECTOR('',#26825,10.);
#7656=VECTOR('',#26826,10.);
#7657=VECTOR('',#26827,10.);
#7658=VECTOR('',#26830,10.);
#7659=VECTOR('',#26831,10.);
#7660=VECTOR('',#26832,10.);
#7661=VECTOR('',#26835,10.);
#7662=VECTOR('',#26836,10.);
#9611=VERTEX_POINT('',#48026);
#9612=VERTEX_POINT('',#48028);
#9613=VERTEX_POINT('',#48032);
#9614=VERTEX_POINT('',#48033);
#9615=VERTEX_POINT('',#48035);
#9616=VERTEX_POINT('',#48037);
#9617=VERTEX_POINT('',#48041);
#9618=VERTEX_POINT('',#48043);
#9619=VERTEX_POINT('',#48047);
#9620=VERTEX_POINT('',#48049);
#12504=EDGE_CURVE('',#9611,#9611,#3951,.T.);
#12505=EDGE_CURVE('',#9611,#9612,#5769,.T.);
#12506=EDGE_CURVE('',#9612,#9612,#3952,.T.);
#12507=EDGE_CURVE('',#9613,#9614,#5770,.T.);
#12508=EDGE_CURVE('',#9613,#9615,#5771,.T.);
#12509=EDGE_CURVE('',#9616,#9615,#5772,.T.);
#12510=EDGE_CURVE('',#9614,#9616,#5773,.T.);
#12511=EDGE_CURVE('',#9614,#9617,#5774,.T.);
#12512=EDGE_CURVE('',#9618,#9616,#5775,.T.);
#12513=EDGE_CURVE('',#9617,#9618,#5776,.T.);
#12514=EDGE_CURVE('',#9617,#9619,#5777,.T.);
#12515=EDGE_CURVE('',#9620,#9618,#5778,.T.);
#12516=EDGE_CURVE('',#9619,#9620,#5779,.T.);
#12517=EDGE_CURVE('',#9619,#9613,#5780,.T.);
#12518=EDGE_CURVE('',#9615,#9620,#5781,.T.);
#18241=ORIENTED_EDGE('',*,*,#12504,.F.);
#18242=ORIENTED_EDGE('',*,*,#12505,.T.);
#18243=ORIENTED_EDGE('',*,*,#12506,.F.);
#18244=ORIENTED_EDGE('',*,*,#12505,.F.);
#18245=ORIENTED_EDGE('',*,*,#12507,.F.);
#18246=ORIENTED_EDGE('',*,*,#12508,.T.);
#18247=ORIENTED_EDGE('',*,*,#12509,.F.);
#18248=ORIENTED_EDGE('',*,*,#12510,.F.);
#18249=ORIENTED_EDGE('',*,*,#12511,.F.);
#18250=ORIENTED_EDGE('',*,*,#12510,.T.);
#18251=ORIENTED_EDGE('',*,*,#12512,.F.);
#18252=ORIENTED_EDGE('',*,*,#12513,.F.);
#18253=ORIENTED_EDGE('',*,*,#12514,.F.);
#18254=ORIENTED_EDGE('',*,*,#12513,.T.);
#18255=ORIENTED_EDGE('',*,*,#12515,.F.);
#18256=ORIENTED_EDGE('',*,*,#12516,.F.);
#18257=ORIENTED_EDGE('',*,*,#12517,.F.);
#18258=ORIENTED_EDGE('',*,*,#12516,.T.);
#18259=ORIENTED_EDGE('',*,*,#12518,.F.);
#18260=ORIENTED_EDGE('',*,*,#12508,.F.);
#18261=ORIENTED_EDGE('',*,*,#12518,.T.);
#18262=ORIENTED_EDGE('',*,*,#12515,.T.);
#18263=ORIENTED_EDGE('',*,*,#12512,.T.);
#18264=ORIENTED_EDGE('',*,*,#12509,.T.);
#18265=ORIENTED_EDGE('',*,*,#12506,.T.);
#18266=ORIENTED_EDGE('',*,*,#12517,.T.);
#18267=ORIENTED_EDGE('',*,*,#12507,.T.);
#18268=ORIENTED_EDGE('',*,*,#12511,.T.);
#18269=ORIENTED_EDGE('',*,*,#12514,.T.);
#18270=ORIENTED_EDGE('',*,*,#12504,.T.);
#19028=PLANE('',#21813);
#19029=PLANE('',#21814);
#19030=PLANE('',#21815);
#19031=PLANE('',#21816);
#19032=PLANE('',#21817);
#19033=PLANE('',#21818);
#20051=ADVANCED_FACE('',(#2194),#1186,.F.);
#20052=ADVANCED_FACE('',(#2195),#19028,.T.);
#20053=ADVANCED_FACE('',(#2196),#19029,.T.);
#20054=ADVANCED_FACE('',(#2197),#19030,.T.);
#20055=ADVANCED_FACE('',(#2198),#19031,.T.);
#20056=ADVANCED_FACE('',(#2199,#723),#19032,.T.);
#20057=ADVANCED_FACE('',(#2200,#724),#19033,.F.);
#20130=CLOSED_SHELL('',(#20051,#20052,#20053,#20054,#20055,#20056,#20057));
#21809=AXIS2_PLACEMENT_3D('',#48024,#26808,#26809);
#21810=AXIS2_PLACEMENT_3D('',#48025,#26810,#26811);
#21811=AXIS2_PLACEMENT_3D('',#48027,#26812,#26813);
#21812=AXIS2_PLACEMENT_3D('',#48030,#26815,#26816);
#21813=AXIS2_PLACEMENT_3D('',#48031,#26817,#26818);
#21814=AXIS2_PLACEMENT_3D('',#48040,#26823,#26824);
#21815=AXIS2_PLACEMENT_3D('',#48046,#26828,#26829);
#21816=AXIS2_PLACEMENT_3D('',#48052,#26833,#26834);
#21817=AXIS2_PLACEMENT_3D('',#48055,#26837,#26838);
#21818=AXIS2_PLACEMENT_3D('',#48056,#26839,#26840);
#26808=DIRECTION('axis',(0.,0.,1.));
#26809=DIRECTION('refdir',(1.,0.,0.));
#26810=DIRECTION('center_axis',(0.,1.,0.));
#26811=DIRECTION('ref_axis',(1.,0.,0.));
#26812=DIRECTION('center_axis',(0.,1.,0.));
#26813=DIRECTION('ref_axis',(1.,0.,0.));
#26814=DIRECTION('',(0.,1.,0.));
#26815=DIRECTION('center_axis',(0.,-1.,0.));
#26816=DIRECTION('ref_axis',(1.,0.,0.));
#26817=DIRECTION('center_axis',(-1.,0.,0.));
#26818=DIRECTION('ref_axis',(0.,0.,1.));
#26819=DIRECTION('',(0.,0.,-1.));
#26820=DIRECTION('',(0.,1.,0.));
#26821=DIRECTION('',(0.,0.,1.));
#26822=DIRECTION('',(0.,1.,0.));
#26823=DIRECTION('center_axis',(0.,0.,-1.));
#26824=DIRECTION('ref_axis',(-1.,0.,0.));
#26825=DIRECTION('',(1.,0.,0.));
#26826=DIRECTION('',(-1.,0.,0.));
#26827=DIRECTION('',(0.,1.,0.));
#26828=DIRECTION('center_axis',(1.,0.,0.));
#26829=DIRECTION('ref_axis',(0.,0.,-1.));
#26830=DIRECTION('',(0.,0.,1.));
#26831=DIRECTION('',(0.,0.,-1.));
#26832=DIRECTION('',(0.,1.,0.));
#26833=DIRECTION('center_axis',(0.,0.,1.));
#26834=DIRECTION('ref_axis',(1.,0.,0.));
#26835=DIRECTION('',(-1.,0.,0.));
#26836=DIRECTION('',(1.,0.,0.));
#26837=DIRECTION('center_axis',(0.,1.,0.));
#26838=DIRECTION('ref_axis',(0.,0.,1.));
#26839=DIRECTION('center_axis',(0.,1.,0.));
#26840=DIRECTION('ref_axis',(1.,0.,0.));
#48024=CARTESIAN_POINT('',(0.,0.,0.));
#48025=CARTESIAN_POINT('Origin',(74.9879498948689,0.,53.0228109606356));
#48026=CARTESIAN_POINT('',(57.4879498948689,0.,53.0228109606356));
#48027=CARTESIAN_POINT('Origin',(74.9879498948689,0.,53.0228109606356));
#48028=CARTESIAN_POINT('',(57.4879498948689,15.,53.0228109606356));
#48029=CARTESIAN_POINT('',(57.4879498948689,0.,53.0228109606356));
#48030=CARTESIAN_POINT('Origin',(74.9879498948689,15.,53.0228109606356));
#48031=CARTESIAN_POINT('Origin',(0.,0.,0.));
#48032=CARTESIAN_POINT('',(0.,0.,85.));
#48033=CARTESIAN_POINT('',(0.,0.,0.));
#48034=CARTESIAN_POINT('',(0.,0.,85.));
#48035=CARTESIAN_POINT('',(0.,15.,85.));
#48036=CARTESIAN_POINT('',(0.,0.,85.));
#48037=CARTESIAN_POINT('',(0.,15.,0.));
#48038=CARTESIAN_POINT('',(0.,15.,85.));
#48039=CARTESIAN_POINT('',(0.,0.,0.));
#48040=CARTESIAN_POINT('Origin',(150.,0.,0.));
#48041=CARTESIAN_POINT('',(150.,0.,0.));
#48042=CARTESIAN_POINT('',(0.,0.,0.));
#48043=CARTESIAN_POINT('',(150.,15.,0.));
#48044=CARTESIAN_POINT('',(0.,15.,0.));
#48045=CARTESIAN_POINT('',(150.,0.,0.));
#48046=CARTESIAN_POINT('Origin',(150.,0.,85.));
#48047=CARTESIAN_POINT('',(150.,0.,85.));
#48048=CARTESIAN_POINT('',(150.,0.,0.));
#48049=CARTESIAN_POINT('',(150.,15.,85.));
#48050=CARTESIAN_POINT('',(150.,15.,0.));
#48051=CARTESIAN_POINT('',(150.,0.,85.));
#48052=CARTESIAN_POINT('Origin',(0.,0.,85.));
#48053=CARTESIAN_POINT('',(150.,0.,85.));
#48054=CARTESIAN_POINT('',(150.,15.,85.));
#48055=CARTESIAN_POINT('Origin',(75.,15.,42.5));
#48056=CARTESIAN_POINT('Origin',(75.,0.,42.5));
#48352=UNCERTAINTY_MEASURE_WITH_UNIT(LENGTH_MEASURE(0.01),#48370,
'DISTANCE_ACCURACY_VALUE',
'Maximum model space distance between geometric entities at asserted c
onnectivities');
#48356=UNCERTAINTY_MEASURE_WITH_UNIT(LENGTH_MEASURE(0.01),#48370,
'DISTANCE_ACCURACY_VALUE',
'Maximum model space distance between geometric entities at asserted c
onnectivities');
#48365=(
GEOMETRIC_REPRESENTATION_CONTEXT(3)
GLOBAL_UNCERTAINTY_ASSIGNED_CONTEXT((#48352))
GLOBAL_UNIT_ASSIGNED_CONTEXT((#48370,#48372,#48373))
REPRESENTATION_CONTEXT('','3D')
);
#48369=(
GEOMETRIC_REPRESENTATION_CONTEXT(3)
GLOBAL_UNCERTAINTY_ASSIGNED_CONTEXT((#48356))
GLOBAL_UNIT_ASSIGNED_CONTEXT((#48370,#48372,#48373))
REPRESENTATION_CONTEXT('','3D')
);
#48370=(
LENGTH_UNIT()
NAMED_UNIT(*)
SI_UNIT(.MILLI.,.METRE.)
);
#48372=(
NAMED_UNIT(*)
PLANE_ANGLE_UNIT()
SI_UNIT($,.RADIAN.)
);
#48373=(
NAMED_UNIT(*)
SI_UNIT($,.STERADIAN.)
SOLID_ANGLE_UNIT()
);
#48382=SHAPE_DEFINITION_REPRESENTATION(#48394,#48420);
#48394=PRODUCT_DEFINITION_SHAPE('',$,#48433);
#48420=SHAPE_REPRESENTATION('',(#21809),#48365);
#48424=PRODUCT_DEFINITION_CONTEXT('part definition',#48462,'design');
#48433=PRODUCT_DEFINITION('Front_Block','Front_Block',#48445,#48424);
#48445=PRODUCT_DEFINITION_FORMATION('',$,#48472);
#48462=APPLICATION_CONTEXT(
'Core Data for Automotive Mechanical Design Process');
#48463=PRODUCT_CONTEXT('part definition',#48462,'mechanical');
#48472=PRODUCT('Front_Block','Front_Block',$,(#48463));
#48490=COLOUR_RGB('Dark Blue',0.08,0.2,0.34);
#48491=FILL_AREA_STYLE_COLOUR('',#48490);
#48492=FILL_AREA_STYLE('',(#48491));
#48493=SURFACE_STYLE_FILL_AREA(#48492);
#48494=SURFACE_SIDE_STYLE('',(#48493));
#48495=SURFACE_STYLE_USAGE(.BOTH.,#48494);
#48496=PRESENTATION_STYLE_ASSIGNMENT((#48495));
ENDSEC;
END-ISO-10303-21;
